ISO-10303-21;
HEADER;
/* Generated by software containing ST-Developer
 * from STEP Tools, Inc. (www.steptools.com) 
 */

FILE_DESCRIPTION(
/* description */ (''),
/* implementation_level */ '2;1');

FILE_NAME(
/* name */ 'Hexagon Thin Nut DIN 439-2 - M5 x 0.8 Steel 6 Plain v1.step',
/* time_stamp */ '2026-10-12T15:37:13-07:00',
/* author */ (''),
/* organization */ (''),
/* preprocessor_version */ 'ST-DEVELOPER v20.2',
/* originating_system */ 'Autodesk Translation Framework v15.15.0.0',
/* authorisation */ '');

FILE_SCHEMA (('AUTOMOTIVE_DESIGN { 1 0 10303 214 3 1 1 }'));
ENDSEC;

DATA;
#10=MECHANICAL_DESIGN_GEOMETRIC_PRESENTATION_REPRESENTATION('',(#336),#36460);
#109=SHAPE_REPRESENTATION_RELATIONSHIP('SRR','None',#36521,#122);
#122=ADVANCED_BREP_SHAPE_REPRESENTATION('',(#368),#36450);
#163=FACE_BOUND('',#1997,.T.);
#164=FACE_BOUND('',#2000,.T.);
#275=(
BOUNDED_CURVE()
B_SPLINE_CURVE(2,(#34670,#34671,#34672),.UNSPECIFIED.,.F.,.F.)
B_SPLINE_CURVE_WITH_KNOTS((3,3),(0.000209851267233562,0.467659076247017),
 .UNSPECIFIED.)
CURVE()
GEOMETRIC_REPRESENTATION_ITEM()
RATIONAL_B_SPLINE_CURVE((1.00013898062186,1.15486101937814,1.00013898062186))
REPRESENTATION_ITEM('')
);
#276=(
BOUNDED_CURVE()
B_SPLINE_CURVE(2,(#34675,#34676,#34677),.UNSPECIFIED.,.F.,.F.)
B_SPLINE_CURVE_WITH_KNOTS((3,3),(0.000209851267233844,0.467659076247017),
 .UNSPECIFIED.)
CURVE()
GEOMETRIC_REPRESENTATION_ITEM()
RATIONAL_B_SPLINE_CURVE((1.00013898062186,1.15486101937814,1.00013898062186))
REPRESENTATION_ITEM('')
);
#277=(
BOUNDED_CURVE()
B_SPLINE_CURVE(2,(#34680,#34681,#34682),.UNSPECIFIED.,.F.,.F.)
B_SPLINE_CURVE_WITH_KNOTS((3,3),(0.000209851267233554,0.467659076247016),
 .UNSPECIFIED.)
CURVE()
GEOMETRIC_REPRESENTATION_ITEM()
RATIONAL_B_SPLINE_CURVE((1.00013898062186,1.15486101937814,1.00013898062186))
REPRESENTATION_ITEM('')
);
#278=(
BOUNDED_CURVE()
B_SPLINE_CURVE(2,(#34685,#34686,#34687),.UNSPECIFIED.,.F.,.F.)
B_SPLINE_CURVE_WITH_KNOTS((3,3),(0.000209851267233599,0.467659076247016),
 .UNSPECIFIED.)
CURVE()
GEOMETRIC_REPRESENTATION_ITEM()
RATIONAL_B_SPLINE_CURVE((1.00013898062186,1.15486101937814,1.00013898062186))
REPRESENTATION_ITEM('')
);
#279=(
BOUNDED_CURVE()
B_SPLINE_CURVE(2,(#34691,#34692,#34693),.UNSPECIFIED.,.F.,.F.)
B_SPLINE_CURVE_WITH_KNOTS((3,3),(1.01019060757112,1.41893400293227),
 .UNSPECIFIED.)
CURVE()
GEOMETRIC_REPRESENTATION_ITEM()
RATIONAL_B_SPLINE_CURVE((1.78107349850061,1.78107349850061,1.65319817466611))
REPRESENTATION_ITEM('')
);
#280=(
BOUNDED_CURVE()
B_SPLINE_CURVE(2,(#34698,#34699,#34700),.UNSPECIFIED.,.F.,.F.)
B_SPLINE_CURVE_WITH_KNOTS((3,3),(0.601447212209968,1.01019060757112),
 .UNSPECIFIED.)
CURVE()
GEOMETRIC_REPRESENTATION_ITEM()
RATIONAL_B_SPLINE_CURVE((1.65319817466611,1.78107349850061,1.78107349850061))
REPRESENTATION_ITEM('')
);
#281=(
BOUNDED_CURVE()
B_SPLINE_CURVE(2,(#34702,#34703,#34704),.UNSPECIFIED.,.F.,.F.)
B_SPLINE_CURVE_WITH_KNOTS((3,3),(0.000209851267233684,0.467659076247016),
 .UNSPECIFIED.)
CURVE()
GEOMETRIC_REPRESENTATION_ITEM()
RATIONAL_B_SPLINE_CURVE((1.00013898062186,1.15486101937814,1.00013898062186))
REPRESENTATION_ITEM('')
);
#282=(
BOUNDED_CURVE()
B_SPLINE_CURVE(2,(#34705,#34706,#34707),.UNSPECIFIED.,.F.,.F.)
B_SPLINE_CURVE_WITH_KNOTS((3,3),(0.000209851267233646,0.467659076247016),
 .UNSPECIFIED.)
CURVE()
GEOMETRIC_REPRESENTATION_ITEM()
RATIONAL_B_SPLINE_CURVE((1.00013898062186,1.15486101937814,1.00013898062186))
REPRESENTATION_ITEM('')
);
#283=(
BOUNDED_CURVE()
B_SPLINE_CURVE(2,(#34708,#34709,#34710),.UNSPECIFIED.,.F.,.F.)
B_SPLINE_CURVE_WITH_KNOTS((3,3),(0.000209851267233851,0.467659076247016),
 .UNSPECIFIED.)
CURVE()
GEOMETRIC_REPRESENTATION_ITEM()
RATIONAL_B_SPLINE_CURVE((1.00013898062186,1.15486101937814,1.00013898062186))
REPRESENTATION_ITEM('')
);
#284=(
BOUNDED_CURVE()
B_SPLINE_CURVE(2,(#34713,#34714,#34715),.UNSPECIFIED.,.F.,.F.)
B_SPLINE_CURVE_WITH_KNOTS((3,3),(0.000209851267233802,0.467659076247016),
 .UNSPECIFIED.)
CURVE()
GEOMETRIC_REPRESENTATION_ITEM()
RATIONAL_B_SPLINE_CURVE((1.00013898062186,1.15486101937814,1.00013898062186))
REPRESENTATION_ITEM('')
);
#285=(
BOUNDED_CURVE()
B_SPLINE_CURVE(2,(#34719,#34720,#34721),.UNSPECIFIED.,.F.,.F.)
B_SPLINE_CURVE_WITH_KNOTS((3,3),(-1.50076840907249,-1.07539867696182),
 .UNSPECIFIED.)
CURVE()
GEOMETRIC_REPRESENTATION_ITEM()
RATIONAL_B_SPLINE_CURVE((1.71537600115701,1.84806079660852,1.84806079660852))
REPRESENTATION_ITEM('')
);
#286=(
BOUNDED_CURVE()
B_SPLINE_CURVE(2,(#34723,#34724,#34725),.UNSPECIFIED.,.F.,.F.)
B_SPLINE_CURVE_WITH_KNOTS((3,3),(-1.07539867696182,-0.650028944851149),
 .UNSPECIFIED.)
CURVE()
GEOMETRIC_REPRESENTATION_ITEM()
RATIONAL_B_SPLINE_CURVE((1.84806079660852,1.84806079660852,1.71537600115701))
REPRESENTATION_ITEM('')
);
#287=(
BOUNDED_CURVE()
B_SPLINE_CURVE(2,(#34729,#34730,#34731),.UNSPECIFIED.,.F.,.F.)
B_SPLINE_CURVE_WITH_KNOTS((3,3),(0.000209851267233587,0.467659076247016),
 .UNSPECIFIED.)
CURVE()
GEOMETRIC_REPRESENTATION_ITEM()
RATIONAL_B_SPLINE_CURVE((1.00013898062186,1.15486101937814,1.00013898062186))
REPRESENTATION_ITEM('')
);
#288=(
BOUNDED_CURVE()
B_SPLINE_CURVE(2,(#34734,#34735,#34736),.UNSPECIFIED.,.F.,.F.)
B_SPLINE_CURVE_WITH_KNOTS((3,3),(0.000209851267233473,0.467659076247016),
 .UNSPECIFIED.)
CURVE()
GEOMETRIC_REPRESENTATION_ITEM()
RATIONAL_B_SPLINE_CURVE((1.00013898062186,1.15486101937814,1.00013898062186))
REPRESENTATION_ITEM('')
);
#315=CONICAL_SURFACE('',#11911,2.110288568297,0.5235987755983);
#316=CONICAL_SURFACE('',#11914,2.110288568297,0.5235987755983);
#317=CONICAL_SURFACE('',#11919,4.27,1.0471975511966);
#318=CONICAL_SURFACE('',#11927,4.27,1.0471975511966);
#336=STYLED_ITEM('',(#36599),#368);
#368=MANIFOLD_SOLID_BREP('Body1',#11272);
#525=PLANE('',#11917);
#526=PLANE('',#11918);
#527=PLANE('',#11921);
#528=PLANE('',#11922);
#529=PLANE('',#11923);
#530=PLANE('',#11924);
#531=PLANE('',#11925);
#532=PLANE('',#11928);
#1342=FACE_OUTER_BOUND('',#1987,.T.);
#1343=FACE_OUTER_BOUND('',#1988,.T.);
#1344=FACE_OUTER_BOUND('',#1989,.T.);
#1345=FACE_OUTER_BOUND('',#1990,.T.);
#1346=FACE_OUTER_BOUND('',#1991,.T.);
#1347=FACE_OUTER_BOUND('',#1992,.T.);
#1348=FACE_OUTER_BOUND('',#1993,.T.);
#1349=FACE_OUTER_BOUND('',#1994,.T.);
#1350=FACE_OUTER_BOUND('',#1995,.T.);
#1351=FACE_OUTER_BOUND('',#1996,.T.);
#1352=FACE_OUTER_BOUND('',#1998,.T.);
#1353=FACE_OUTER_BOUND('',#1999,.T.);
#1354=FACE_OUTER_BOUND('',#2001,.T.);
#1987=EDGE_LOOP('',(#8882,#8883,#8884,#8885));
#1988=EDGE_LOOP('',(#8886,#8887,#8888,#8889));
#1989=EDGE_LOOP('',(#8890,#8891,#8892,#8893));
#1990=EDGE_LOOP('',(#8894,#8895,#8896,#8897));
#1991=EDGE_LOOP('',(#8898,#8899,#8900,#8901,#8902,#8903,#8904,#8905,#8906,
#8907));
#1992=EDGE_LOOP('',(#8908,#8909,#8910,#8911));
#1993=EDGE_LOOP('',(#8912,#8913,#8914,#8915,#8916,#8917));
#1994=EDGE_LOOP('',(#8918,#8919,#8920,#8921));
#1995=EDGE_LOOP('',(#8922,#8923,#8924,#8925));
#1996=EDGE_LOOP('',(#8926));
#1997=EDGE_LOOP('',(#8927));
#1998=EDGE_LOOP('',(#8928,#8929,#8930,#8931,#8932,#8933,#8934,#8935,#8936,
#8937));
#1999=EDGE_LOOP('',(#8938));
#2000=EDGE_LOOP('',(#8939));
#2001=EDGE_LOOP('',(#8940,#8941,#8942,#8943));
#2787=LINE('',#34657,#3733);
#2788=LINE('',#34663,#3734);
#2789=LINE('',#34668,#3735);
#2790=LINE('',#34674,#3736);
#2791=LINE('',#34684,#3737);
#2792=LINE('',#34695,#3738);
#2793=LINE('',#34716,#3739);
#2794=LINE('',#34726,#3740);
#2795=LINE('',#34732,#3741);
#2796=LINE('',#34741,#3742);
#2797=LINE('',#34744,#3743);
#3733=VECTOR('',#13786,2.110288568297);
#3734=VECTOR('',#13793,2.110288568297);
#3735=VECTOR('',#13798,10.);
#3736=VECTOR('',#13799,10.);
#3737=VECTOR('',#13802,10.);
#3738=VECTOR('',#13805,4.27);
#3739=VECTOR('',#13810,10.);
#3740=VECTOR('',#13813,10.);
#3741=VECTOR('',#13816,10.);
#3742=VECTOR('',#13825,4.27);
#3743=VECTOR('',#13830,2.117);
#4396=CIRCLE('',#11912,2.117);
#4397=CIRCLE('',#11913,2.5);
#4398=CIRCLE('',#11915,2.117);
#4399=CIRCLE('',#11916,2.5);
#4400=CIRCLE('',#11920,3.92);
#4401=CIRCLE('',#11926,3.92);
#5133=VERTEX_POINT('',#34654);
#5134=VERTEX_POINT('',#34656);
#5135=VERTEX_POINT('',#34660);
#5136=VERTEX_POINT('',#34662);
#5137=VERTEX_POINT('',#34666);
#5138=VERTEX_POINT('',#34667);
#5139=VERTEX_POINT('',#34669);
#5140=VERTEX_POINT('',#34673);
#5141=VERTEX_POINT('',#34679);
#5142=VERTEX_POINT('',#34683);
#5143=VERTEX_POINT('',#34689);
#5144=VERTEX_POINT('',#34690);
#5145=VERTEX_POINT('',#34694);
#5146=VERTEX_POINT('',#34697);
#5147=VERTEX_POINT('',#34701);
#5148=VERTEX_POINT('',#34712);
#5149=VERTEX_POINT('',#34718);
#5150=VERTEX_POINT('',#34722);
#5151=VERTEX_POINT('',#34728);
#5152=VERTEX_POINT('',#34738);
#6472=EDGE_CURVE('',#5133,#5133,#4396,.T.);
#6473=EDGE_CURVE('',#5133,#5134,#2787,.T.);
#6474=EDGE_CURVE('',#5134,#5134,#4397,.T.);
#6475=EDGE_CURVE('',#5135,#5135,#4398,.T.);
#6476=EDGE_CURVE('',#5135,#5136,#2788,.T.);
#6477=EDGE_CURVE('',#5136,#5136,#4399,.T.);
#6478=EDGE_CURVE('',#5137,#5138,#2789,.T.);
#6479=EDGE_CURVE('',#5139,#5137,#275,.T.);
#6480=EDGE_CURVE('',#5140,#5139,#2790,.T.);
#6481=EDGE_CURVE('',#5138,#5140,#276,.T.);
#6482=EDGE_CURVE('',#5141,#5139,#277,.T.);
#6483=EDGE_CURVE('',#5141,#5142,#2791,.T.);
#6484=EDGE_CURVE('',#5140,#5142,#278,.T.);
#6485=EDGE_CURVE('',#5143,#5144,#279,.F.);
#6486=EDGE_CURVE('',#5144,#5145,#2792,.T.);
#6487=EDGE_CURVE('',#5145,#5145,#4400,.T.);
#6488=EDGE_CURVE('',#5144,#5146,#280,.F.);
#6489=EDGE_CURVE('',#5146,#5147,#281,.T.);
#6490=EDGE_CURVE('',#5147,#5141,#282,.T.);
#6491=EDGE_CURVE('',#5137,#5143,#283,.T.);
#6492=EDGE_CURVE('',#5148,#5138,#284,.T.);
#6493=EDGE_CURVE('',#5143,#5148,#2793,.T.);
#6494=EDGE_CURVE('',#5149,#5148,#285,.F.);
#6495=EDGE_CURVE('',#5150,#5149,#286,.F.);
#6496=EDGE_CURVE('',#5146,#5150,#2794,.T.);
#6497=EDGE_CURVE('',#5151,#5150,#287,.T.);
#6498=EDGE_CURVE('',#5147,#5151,#2795,.T.);
#6499=EDGE_CURVE('',#5142,#5151,#288,.T.);
#6500=EDGE_CURVE('',#5152,#5152,#4401,.T.);
#6501=EDGE_CURVE('',#5149,#5152,#2796,.T.);
#6502=EDGE_CURVE('',#5135,#5133,#2797,.T.);
#8882=ORIENTED_EDGE('',*,*,#6472,.F.);
#8883=ORIENTED_EDGE('',*,*,#6473,.T.);
#8884=ORIENTED_EDGE('',*,*,#6474,.F.);
#8885=ORIENTED_EDGE('',*,*,#6473,.F.);
#8886=ORIENTED_EDGE('',*,*,#6475,.F.);
#8887=ORIENTED_EDGE('',*,*,#6476,.T.);
#8888=ORIENTED_EDGE('',*,*,#6477,.F.);
#8889=ORIENTED_EDGE('',*,*,#6476,.F.);
#8890=ORIENTED_EDGE('',*,*,#6478,.F.);
#8891=ORIENTED_EDGE('',*,*,#6479,.F.);
#8892=ORIENTED_EDGE('',*,*,#6480,.F.);
#8893=ORIENTED_EDGE('',*,*,#6481,.F.);
#8894=ORIENTED_EDGE('',*,*,#6480,.T.);
#8895=ORIENTED_EDGE('',*,*,#6482,.F.);
#8896=ORIENTED_EDGE('',*,*,#6483,.T.);
#8897=ORIENTED_EDGE('',*,*,#6484,.F.);
#8898=ORIENTED_EDGE('',*,*,#6485,.T.);
#8899=ORIENTED_EDGE('',*,*,#6486,.T.);
#8900=ORIENTED_EDGE('',*,*,#6487,.F.);
#8901=ORIENTED_EDGE('',*,*,#6486,.F.);
#8902=ORIENTED_EDGE('',*,*,#6488,.T.);
#8903=ORIENTED_EDGE('',*,*,#6489,.T.);
#8904=ORIENTED_EDGE('',*,*,#6490,.T.);
#8905=ORIENTED_EDGE('',*,*,#6482,.T.);
#8906=ORIENTED_EDGE('',*,*,#6479,.T.);
#8907=ORIENTED_EDGE('',*,*,#6491,.T.);
#8908=ORIENTED_EDGE('',*,*,#6478,.T.);
#8909=ORIENTED_EDGE('',*,*,#6492,.F.);
#8910=ORIENTED_EDGE('',*,*,#6493,.F.);
#8911=ORIENTED_EDGE('',*,*,#6491,.F.);
#8912=ORIENTED_EDGE('',*,*,#6493,.T.);
#8913=ORIENTED_EDGE('',*,*,#6494,.F.);
#8914=ORIENTED_EDGE('',*,*,#6495,.F.);
#8915=ORIENTED_EDGE('',*,*,#6496,.F.);
#8916=ORIENTED_EDGE('',*,*,#6488,.F.);
#8917=ORIENTED_EDGE('',*,*,#6485,.F.);
#8918=ORIENTED_EDGE('',*,*,#6496,.T.);
#8919=ORIENTED_EDGE('',*,*,#6497,.F.);
#8920=ORIENTED_EDGE('',*,*,#6498,.F.);
#8921=ORIENTED_EDGE('',*,*,#6489,.F.);
#8922=ORIENTED_EDGE('',*,*,#6498,.T.);
#8923=ORIENTED_EDGE('',*,*,#6499,.F.);
#8924=ORIENTED_EDGE('',*,*,#6483,.F.);
#8925=ORIENTED_EDGE('',*,*,#6490,.F.);
#8926=ORIENTED_EDGE('',*,*,#6500,.F.);
#8927=ORIENTED_EDGE('',*,*,#6477,.T.);
#8928=ORIENTED_EDGE('',*,*,#6495,.T.);
#8929=ORIENTED_EDGE('',*,*,#6501,.T.);
#8930=ORIENTED_EDGE('',*,*,#6500,.T.);
#8931=ORIENTED_EDGE('',*,*,#6501,.F.);
#8932=ORIENTED_EDGE('',*,*,#6494,.T.);
#8933=ORIENTED_EDGE('',*,*,#6492,.T.);
#8934=ORIENTED_EDGE('',*,*,#6481,.T.);
#8935=ORIENTED_EDGE('',*,*,#6484,.T.);
#8936=ORIENTED_EDGE('',*,*,#6499,.T.);
#8937=ORIENTED_EDGE('',*,*,#6497,.T.);
#8938=ORIENTED_EDGE('',*,*,#6487,.T.);
#8939=ORIENTED_EDGE('',*,*,#6474,.T.);
#8940=ORIENTED_EDGE('',*,*,#6475,.T.);
#8941=ORIENTED_EDGE('',*,*,#6502,.T.);
#8942=ORIENTED_EDGE('',*,*,#6472,.T.);
#8943=ORIENTED_EDGE('',*,*,#6502,.F.);
#10564=CYLINDRICAL_SURFACE('',#11929,2.117);
#10963=ADVANCED_FACE('',(#1342),#315,.F.);
#10964=ADVANCED_FACE('',(#1343),#316,.F.);
#10965=ADVANCED_FACE('',(#1344),#525,.F.);
#10966=ADVANCED_FACE('',(#1345),#526,.F.);
#10967=ADVANCED_FACE('',(#1346),#317,.T.);
#10968=ADVANCED_FACE('',(#1347),#527,.F.);
#10969=ADVANCED_FACE('',(#1348),#528,.F.);
#10970=ADVANCED_FACE('',(#1349),#529,.F.);
#10971=ADVANCED_FACE('',(#1350),#530,.F.);
#10972=ADVANCED_FACE('',(#1351,#163),#531,.T.);
#10973=ADVANCED_FACE('',(#1352),#318,.T.);
#10974=ADVANCED_FACE('',(#1353,#164),#532,.T.);
#10975=ADVANCED_FACE('',(#1354),#10564,.F.);
#11272=CLOSED_SHELL('',(#10963,#10964,#10965,#10966,#10967,#10968,#10969,
#10970,#10971,#10972,#10973,#10974,#10975));
#11910=AXIS2_PLACEMENT_3D('',#34652,#13780,#13781);
#11911=AXIS2_PLACEMENT_3D('',#34653,#13782,#13783);
#11912=AXIS2_PLACEMENT_3D('',#34655,#13784,#13785);
#11913=AXIS2_PLACEMENT_3D('',#34658,#13787,#13788);
#11914=AXIS2_PLACEMENT_3D('',#34659,#13789,#13790);
#11915=AXIS2_PLACEMENT_3D('',#34661,#13791,#13792);
#11916=AXIS2_PLACEMENT_3D('',#34664,#13794,#13795);
#11917=AXIS2_PLACEMENT_3D('',#34665,#13796,#13797);
#11918=AXIS2_PLACEMENT_3D('',#34678,#13800,#13801);
#11919=AXIS2_PLACEMENT_3D('',#34688,#13803,#13804);
#11920=AXIS2_PLACEMENT_3D('',#34696,#13806,#13807);
#11921=AXIS2_PLACEMENT_3D('',#34711,#13808,#13809);
#11922=AXIS2_PLACEMENT_3D('',#34717,#13811,#13812);
#11923=AXIS2_PLACEMENT_3D('',#34727,#13814,#13815);
#11924=AXIS2_PLACEMENT_3D('',#34733,#13817,#13818);
#11925=AXIS2_PLACEMENT_3D('',#34737,#13819,#13820);
#11926=AXIS2_PLACEMENT_3D('',#34739,#13821,#13822);
#11927=AXIS2_PLACEMENT_3D('',#34740,#13823,#13824);
#11928=AXIS2_PLACEMENT_3D('',#34742,#13826,#13827);
#11929=AXIS2_PLACEMENT_3D('',#34743,#13828,#13829);
#13780=DIRECTION('axis',(0.,0.,1.));
#13781=DIRECTION('refdir',(1.,0.,0.));
#13782=DIRECTION('center_axis',(0.,0.,-1.));
#13783=DIRECTION('ref_axis',(-1.,0.,0.));
#13784=DIRECTION('center_axis',(0.,0.,-1.));
#13785=DIRECTION('ref_axis',(-1.,0.,0.));
#13786=DIRECTION('',(0.500000000000001,-6.12323399573678E-17,-0.866025403784438));
#13787=DIRECTION('center_axis',(0.,0.,1.));
#13788=DIRECTION('ref_axis',(-1.,0.,0.));
#13789=DIRECTION('center_axis',(0.,0.,1.));
#13790=DIRECTION('ref_axis',(-1.,0.,0.));
#13791=DIRECTION('center_axis',(0.,0.,1.));
#13792=DIRECTION('ref_axis',(-1.,0.,0.));
#13793=DIRECTION('',(0.500000000000001,6.12323399573678E-17,0.866025403784438));
#13794=DIRECTION('center_axis',(0.,0.,-1.));
#13795=DIRECTION('ref_axis',(-1.,0.,0.));
#13796=DIRECTION('center_axis',(0.499999999999999,-0.866025403784439,0.));
#13797=DIRECTION('ref_axis',(-0.866025403784439,-0.499999999999999,0.));
#13798=DIRECTION('',(0.,0.,1.));
#13799=DIRECTION('',(0.,0.,-1.));
#13800=DIRECTION('center_axis',(1.,-7.20364017026615E-16,0.));
#13801=DIRECTION('ref_axis',(-7.20364017026615E-16,-1.,0.));
#13802=DIRECTION('',(0.,0.,1.));
#13803=DIRECTION('center_axis',(0.,0.,1.));
#13804=DIRECTION('ref_axis',(-1.,0.,0.));
#13805=DIRECTION('',(-0.86602540378444,-1.06057523872491E-16,-0.499999999999998));
#13806=DIRECTION('center_axis',(0.,0.,-1.));
#13807=DIRECTION('ref_axis',(1.,0.,0.));
#13808=DIRECTION('center_axis',(-0.500000000000001,-0.866025403784438,0.));
#13809=DIRECTION('ref_axis',(-0.866025403784438,0.500000000000001,0.));
#13810=DIRECTION('',(0.,0.,1.));
#13811=DIRECTION('center_axis',(-1.,8.4282869694135E-16,0.));
#13812=DIRECTION('ref_axis',(8.4282869694135E-16,1.,0.));
#13813=DIRECTION('',(0.,0.,1.));
#13814=DIRECTION('center_axis',(-0.499999999999999,0.866025403784439,0.));
#13815=DIRECTION('ref_axis',(0.866025403784439,0.499999999999999,0.));
#13816=DIRECTION('',(0.,0.,1.));
#13817=DIRECTION('center_axis',(0.500000000000001,0.866025403784438,0.));
#13818=DIRECTION('ref_axis',(0.866025403784438,-0.500000000000001,0.));
#13819=DIRECTION('center_axis',(0.,0.,1.));
#13820=DIRECTION('ref_axis',(1.,0.,0.));
#13821=DIRECTION('center_axis',(0.,0.,-1.));
#13822=DIRECTION('ref_axis',(1.,0.,0.));
#13823=DIRECTION('center_axis',(0.,0.,-1.));
#13824=DIRECTION('ref_axis',(-1.,0.,0.));
#13825=DIRECTION('',(-0.86602540378444,1.06057523872491E-16,0.499999999999998));
#13826=DIRECTION('center_axis',(0.,0.,-1.));
#13827=DIRECTION('ref_axis',(-1.,0.,0.));
#13828=DIRECTION('center_axis',(0.,0.,-1.));
#13829=DIRECTION('ref_axis',(-1.,0.,0.));
#13830=DIRECTION('',(0.,0.,-1.));
#34652=CARTESIAN_POINT('',(0.,0.,0.));
#34653=CARTESIAN_POINT('Origin',(0.,0.,0.675));
#34654=CARTESIAN_POINT('',(2.117,-2.59257727379495E-16,0.663375459298879));
#34655=CARTESIAN_POINT('Origin',(0.,0.,0.663375459298879));
#34656=CARTESIAN_POINT('',(2.5,-3.06161699786838E-16,-2.77555756156289E-16));
#34657=CARTESIAN_POINT('',(2.110288568297,-2.58435814044217E-16,0.675));
#34658=CARTESIAN_POINT('Origin',(0.,0.,0.));
#34659=CARTESIAN_POINT('Origin',(0.,0.,2.025));
#34660=CARTESIAN_POINT('',(2.117,2.59257727379495E-16,2.03662454070112));
#34661=CARTESIAN_POINT('Origin',(0.,0.,2.03662454070112));
#34662=CARTESIAN_POINT('',(2.5,-3.06161699786838E-16,2.7));
#34663=CARTESIAN_POINT('',(2.110288568297,2.58435814044217E-16,2.025));
#34664=CARTESIAN_POINT('Origin',(0.,0.,2.7));
#34665=CARTESIAN_POINT('Origin',(0.00207392470908813,4.61999953450607,2.7));
#34666=CARTESIAN_POINT('',(6.47240898139264E-15,4.618802153517,0.403453611443332));
#34667=CARTESIAN_POINT('',(6.40757044047557E-15,4.618802153517,2.29654638855667));
#34668=CARTESIAN_POINT('',(6.38378239159465E-15,4.618802153517,2.7));
#34669=CARTESIAN_POINT('',(-4.,2.30940107675851,0.403453611443333));
#34670=CARTESIAN_POINT('Ctrl Pts',(-4.,2.30940107675851,0.403453611443333));
#34671=CARTESIAN_POINT('Ctrl Pts',(-2.,3.46410161513776,-0.263213055223336));
#34672=CARTESIAN_POINT('Ctrl Pts',(6.47240898139264E-15,4.618802153517,
0.403453611443332));
#34673=CARTESIAN_POINT('',(-4.,2.30940107675851,2.29654638855667));
#34674=CARTESIAN_POINT('',(-4.,2.30940107675851,2.7));
#34675=CARTESIAN_POINT('Ctrl Pts',(6.40757044047557E-15,4.618802153517,
2.29654638855667));
#34676=CARTESIAN_POINT('Ctrl Pts',(-1.99999999999999,3.46410161513776,2.96321305522333));
#34677=CARTESIAN_POINT('Ctrl Pts',(-4.,2.30940107675851,2.29654638855667));
#34678=CARTESIAN_POINT('Origin',(-4.,2.31179583873664,2.7));
#34679=CARTESIAN_POINT('',(-4.,-2.3094010767585,0.403453611443332));
#34680=CARTESIAN_POINT('Ctrl Pts',(-4.,-2.3094010767585,0.403453611443332));
#34681=CARTESIAN_POINT('Ctrl Pts',(-4.,3.05311331771918E-15,-0.263213055223334));
#34682=CARTESIAN_POINT('Ctrl Pts',(-4.,2.30940107675851,0.403453611443333));
#34683=CARTESIAN_POINT('',(-4.,-2.3094010767585,2.29654638855667));
#34684=CARTESIAN_POINT('',(-4.,-2.3094010767585,2.7));
#34685=CARTESIAN_POINT('Ctrl Pts',(-4.,2.30940107675851,2.29654638855667));
#34686=CARTESIAN_POINT('Ctrl Pts',(-4.,2.77555756156289E-15,2.96321305522333));
#34687=CARTESIAN_POINT('Ctrl Pts',(-4.,-2.3094010767585,2.29654638855667));
#34688=CARTESIAN_POINT('Origin',(0.,0.,0.202072594216369));
#34689=CARTESIAN_POINT('',(4.,2.3094010767585,0.403453611443332));
#34690=CARTESIAN_POINT('',(4.,2.44929359829471E-16,0.0461880215351717));
#34691=CARTESIAN_POINT('Ctrl Pts',(4.,0.,0.0461880215351717));
#34692=CARTESIAN_POINT('Ctrl Pts',(4.,1.07179676972558,0.0461880215351722));
#34693=CARTESIAN_POINT('Ctrl Pts',(4.,2.30940107676122,0.403453611444119));
#34694=CARTESIAN_POINT('',(3.92,-4.80061545265762E-16,-2.08166817117217E-16));
#34695=CARTESIAN_POINT('',(4.27,5.2292418323592E-16,0.202072594216369));
#34696=CARTESIAN_POINT('Origin',(0.,0.,0.));
#34697=CARTESIAN_POINT('',(4.,-2.30940107675851,0.403453611443332));
#34698=CARTESIAN_POINT('Ctrl Pts',(4.,-2.30940107676123,0.40345361144412));
#34699=CARTESIAN_POINT('Ctrl Pts',(4.,-1.07179676972559,0.0461880215351713));
#34700=CARTESIAN_POINT('Ctrl Pts',(4.,0.,0.0461880215351717));
#34701=CARTESIAN_POINT('',(-4.62343916228259E-15,-4.618802153517,0.403453611443332));
#34702=CARTESIAN_POINT('Ctrl Pts',(4.,-2.30940107675851,0.403453611443332));
#34703=CARTESIAN_POINT('Ctrl Pts',(2.,-3.46410161513775,-0.263213055223336));
#34704=CARTESIAN_POINT('Ctrl Pts',(-4.62343916228259E-15,-4.618802153517,
0.403453611443332));
#34705=CARTESIAN_POINT('Ctrl Pts',(-4.6713134644614E-15,-4.618802153517,
0.403453611443332));
#34706=CARTESIAN_POINT('Ctrl Pts',(-2.,-3.46410161513775,-0.263213055223335));
#34707=CARTESIAN_POINT('Ctrl Pts',(-4.,-2.3094010767585,0.403453611443332));
#34708=CARTESIAN_POINT('Ctrl Pts',(6.38831555038924E-15,4.618802153517,
0.403453611443332));
#34709=CARTESIAN_POINT('Ctrl Pts',(2.,3.46410161513775,-0.263213055223334));
#34710=CARTESIAN_POINT('Ctrl Pts',(4.,2.3094010767585,0.403453611443332));
#34711=CARTESIAN_POINT('Origin',(4.00207392470908,2.30820369576943,2.7));
#34712=CARTESIAN_POINT('',(4.,2.3094010767585,2.29654638855667));
#34713=CARTESIAN_POINT('Ctrl Pts',(4.,2.3094010767585,2.29654638855667));
#34714=CARTESIAN_POINT('Ctrl Pts',(2.,3.46410161513775,2.96321305522333));
#34715=CARTESIAN_POINT('Ctrl Pts',(6.31419352837025E-15,4.618802153517,
2.29654638855667));
#34716=CARTESIAN_POINT('',(4.,2.3094010767585,2.7));
#34717=CARTESIAN_POINT('Origin',(4.,-2.31179583873664,2.7));
#34718=CARTESIAN_POINT('',(4.,-9.47417920472595E-17,2.65381197846483));
#34719=CARTESIAN_POINT('Ctrl Pts',(4.,2.30940107676399,2.29654638855508));
#34720=CARTESIAN_POINT('Ctrl Pts',(4.,1.0717967697267,2.65381197846483));
#34721=CARTESIAN_POINT('Ctrl Pts',(4.,3.00375135564423E-16,2.65381197846483));
#34722=CARTESIAN_POINT('',(4.,-2.30940107675851,2.29654638855667));
#34723=CARTESIAN_POINT('Ctrl Pts',(4.,3.00375135564423E-16,2.65381197846483));
#34724=CARTESIAN_POINT('Ctrl Pts',(4.,-1.0717967697267,2.65381197846483));
#34725=CARTESIAN_POINT('Ctrl Pts',(4.,-2.309401076764,2.29654638855508));
#34726=CARTESIAN_POINT('',(4.,-2.30940107675851,2.7));
#34727=CARTESIAN_POINT('Origin',(-0.00207392470908535,-4.61999953450607,
2.7));
#34728=CARTESIAN_POINT('',(-5.55275774471924E-15,-4.618802153517,2.29654638855667));
#34729=CARTESIAN_POINT('Ctrl Pts',(-5.55275774471924E-15,-4.618802153517,
2.29654638855667));
#34730=CARTESIAN_POINT('Ctrl Pts',(2.,-3.46410161513776,2.96321305522334));
#34731=CARTESIAN_POINT('Ctrl Pts',(4.,-2.30940107675851,2.29654638855667));
#34732=CARTESIAN_POINT('',(-4.44089209850063E-15,-4.618802153517,2.7));
#34733=CARTESIAN_POINT('Origin',(-4.00207392470908,-2.30820369576943,2.7));
#34734=CARTESIAN_POINT('Ctrl Pts',(-4.,-2.3094010767585,2.29654638855667));
#34735=CARTESIAN_POINT('Ctrl Pts',(-2.,-3.46410161513775,2.96321305522333));
#34736=CARTESIAN_POINT('Ctrl Pts',(-5.73341293170963E-15,-4.618802153517,
2.29654638855667));
#34737=CARTESIAN_POINT('Origin',(-3.92,0.,2.7));
#34738=CARTESIAN_POINT('',(3.92,-4.80061545265762E-16,2.7));
#34739=CARTESIAN_POINT('Origin',(0.,0.,2.7));
#34740=CARTESIAN_POINT('Origin',(0.,0.,2.49792740578363));
#34741=CARTESIAN_POINT('',(4.27,-5.2292418323592E-16,2.49792740578363));
#34742=CARTESIAN_POINT('Origin',(-2.5,0.,0.));
#34743=CARTESIAN_POINT('Origin',(0.,0.,1.35));
#34744=CARTESIAN_POINT('',(2.117,-2.59257727379495E-16,1.35));
#36434=UNCERTAINTY_MEASURE_WITH_UNIT(LENGTH_MEASURE(0.01),#36461,
'DISTANCE_ACCURACY_VALUE',
'Maximum model space distance between geometric entities at asserted c
onnectivities');
#36444=UNCERTAINTY_MEASURE_WITH_UNIT(LENGTH_MEASURE(0.01),#36461,
'DISTANCE_ACCURACY_VALUE',
'Maximum model space distance between geometric entities at asserted c
onnectivities');
#36450=(
GEOMETRIC_REPRESENTATION_CONTEXT(3)
GLOBAL_UNCERTAINTY_ASSIGNED_CONTEXT((#36434))
GLOBAL_UNIT_ASSIGNED_CONTEXT((#36461,#36463,#36464))
REPRESENTATION_CONTEXT('','3D')
);
#36460=(
GEOMETRIC_REPRESENTATION_CONTEXT(3)
GLOBAL_UNCERTAINTY_ASSIGNED_CONTEXT((#36444))
GLOBAL_UNIT_ASSIGNED_CONTEXT((#36461,#36463,#36464))
REPRESENTATION_CONTEXT('','3D')
);
#36461=(
LENGTH_UNIT()
NAMED_UNIT(*)
SI_UNIT(.MILLI.,.METRE.)
);
#36463=(
NAMED_UNIT(*)
PLANE_ANGLE_UNIT()
SI_UNIT($,.RADIAN.)
);
#36464=(
NAMED_UNIT(*)
SI_UNIT($,.STERADIAN.)
SOLID_ANGLE_UNIT()
);
#36470=SHAPE_DEFINITION_REPRESENTATION(#36485,#36521);
#36485=PRODUCT_DEFINITION_SHAPE('',$,#36537);
#36521=SHAPE_REPRESENTATION('',(#11910),#36450);
#36531=PRODUCT_DEFINITION_CONTEXT('part definition',#36578,'design');
#36537=PRODUCT_DEFINITION('DIN 439-2 - M5 x 0.8 Steel 6 Plain',
'Hexagon Thin Nut DIN 439-2 - M5 x 0.8 Steel 6 Plain v1',#36552,#36531);
#36552=PRODUCT_DEFINITION_FORMATION('',$,#36585);
#36578=APPLICATION_CONTEXT(
'Core Data for Automotive Mechanical Design Process');
#36579=PRODUCT_CONTEXT('part definition',#36578,'mechanical');
#36585=PRODUCT('DIN 439-2 - M5 x 0.8 Steel 6 Plain',
'Hexagon Thin Nut DIN 439-2 - M5 x 0.8 Steel 6 Plain v1',
'Hexagon Thin Nut DIN 439-2 - M5 x 0.8',(#36579));
#36599=PRESENTATION_STYLE_ASSIGNMENT((#36604));
#36604=SURFACE_STYLE_USAGE(.BOTH.,#36609);
#36609=SURFACE_SIDE_STYLE('',(#36614));
#36614=SURFACE_STYLE_FILL_AREA(#36619);
#36619=FILL_AREA_STYLE('Opaque(203,203,203)',(#36624));
#36624=FILL_AREA_STYLE_COLOUR('Opaque(203,203,203)',#36629);
#36629=COLOUR_RGB('Opaque(203,203,203)', 0.72549020, 0.75294118, 0.79215686);
ENDSEC;
END-ISO-10303-21;
